ISO-10303-21;
HEADER;
FILE_DESCRIPTION (('STEP AP214'),
    '1' );
FILE_NAME ('socket head cap screw_iso_ISO 4762 M5 x 16 - 16N.step',
    '2026-10-31T03:46:07',
    ( '' ),
    ( '' ),
    'SwSTEP 2.0',
    'SolidWorks 2026',
    '' );
FILE_SCHEMA (( 'AUTOMOTIVE_DESIGN' ));
ENDSEC;

DATA;
#32=EDGE_CURVE ( 'NONE', #16311, #19722, #7366, .T. ) ;
#35=AXIS2_PLACEMENT_3D ( 'NONE', #14341, #8390, #14444 ) ;
#40=EDGE_LOOP ( 'NONE', ( #2219, #256, #14388 ) ) ;
#49=ORIENTED_EDGE ( 'NONE', *, *, #7796, .F. ) ;
#72=CARTESIAN_POINT ( 'NONE',  ( 5.000000000000002665, 0.000000000000000000, -2.700000000000000622 ) ) ;
#80=DIRECTION ( 'NONE',  ( -0.000000000000000000, 1.287488025362403787E-15, 1.000000000000000000 ) ) ;
#85=DIRECTION ( 'NONE',  ( 0.000000000000000000, 0.000000000000000000, 1.000000000000000000 ) ) ;
#124=CARTESIAN_POINT ( 'NONE',  ( 2.500000000000000000, -1.178949249685214307, 2.042000000000001592 ) ) ;
#132=AXIS2_PLACEMENT_3D ( 'NONE', #19134, #13752, #799 ) ;
#136=DIRECTION ( 'NONE',  ( -1.000000000000000000, -0.000000000000000000, -0.000000000000000000 ) ) ;
#174=ADVANCED_FACE ( 'NONE', ( #20884 ), #9674, .F. ) ;
#196=CARTESIAN_POINT ( 'NONE',  ( 0.000000000000000000, 0.000000000000000000, 0.000000000000000000 ) ) ;
#200=CARTESIAN_POINT ( 'NONE',  ( 2.500000000000000000, -2.357898499370432166, 3.035766082959412415E-15 ) ) ;
#253=CARTESIAN_POINT ( 'NONE',  ( 2.500000000000000000, -1.178949249685218748, -2.041999999999998039 ) ) ;
#256=ORIENTED_EDGE ( 'NONE', *, *, #23484, .F. ) ;
#286=VERTEX_POINT ( 'NONE', #17139 ) ;
#303=( NAMED_UNIT ( * ) PLANE_ANGLE_UNIT ( ) SI_UNIT ( $, .RADIAN. ) );
#311=CARTESIAN_POINT ( 'NONE',  ( 2.500000000000000000, -1.178949249685214307, 2.042000000000001592 ) ) ;
#344=CARTESIAN_POINT ( 'NONE',  ( 5.200000000000002842, 0.000000000000000000, 2.500000000000000444 ) ) ;
#489=DIRECTION ( 'NONE',  ( -1.000000000000000000, -0.000000000000000000, -0.000000000000000000 ) ) ;
#494=CARTESIAN_POINT ( 'NONE',  ( 2.500000000000000000, 2.357898499370431722, -2.818925648462311528E-15 ) ) ;
#521=AXIS2_PLACEMENT_3D ( 'NONE', #1409, #23626, #7438 ) ;
#522=EDGE_CURVE ( 'NONE', #18839, #1157, #6119, .T. ) ;
#659=DIRECTION ( 'NONE',  ( 1.000000000000000000, 0.000000000000000000, 0.000000000000000000 ) ) ;
#704=VECTOR ( 'NONE', #5918, 1000.000000000000114 ) ;
#711=VERTEX_POINT ( 'NONE', #17367 ) ;
#765=ORIENTED_EDGE ( 'NONE', *, *, #20200, .T. ) ;
#779=TOROIDAL_SURFACE ( 'NONE', #11961, 2.700000000000000622, 0.2000000000000000111 ) ;
#785=DIRECTION ( 'NONE',  ( 0.000000000000000000, -0.4999999999999989453, 0.8660254037844391517 ) ) ;
#792=ORIENTED_EDGE ( 'NONE', *, *, #21842, .T. ) ;
#799=DIRECTION ( 'NONE',  ( 0.000000000000000000, 0.000000000000000000, 1.000000000000000000 ) ) ;
#801=CARTESIAN_POINT ( 'NONE',  ( 2.500000000000000000, 2.357898499370431722, -2.818925648462311528E-15 ) ) ;
#863=EDGE_CURVE ( 'NONE', #1754, #12819, #21567, .T. ) ;
#873=ORIENTED_EDGE ( 'NONE', *, *, #18205, .T. ) ;
#881=CIRCLE ( 'NONE', #521, 2.700000000000000622 ) ;
#962=( GEOMETRIC_REPRESENTATION_CONTEXT ( 3 ) GLOBAL_UNCERTAINTY_ASSIGNED_CONTEXT ( ( #11735 ) ) GLOBAL_UNIT_ASSIGNED_CONTEXT ( ( #18533, #303, #5615 ) ) REPRESENTATION_CONTEXT ( 'NONE', 'WORKASPACE' ) );
#968=LINE ( 'NONE', #19434, #7526 ) ;
#978=LINE ( 'NONE', #17529, #19608 ) ;
#1042=PRODUCT_DEFINITION ( 'UNKNOWN', '', #6177, #18456 ) ;
#1057=CIRCLE ( 'NONE', #23027, 4.250000000000000000 ) ;
#1073=EDGE_CURVE ( 'NONE', #7880, #21824, #10292, .T. ) ;
#1100=VECTOR ( 'NONE', #136, 1000.000000000000000 ) ;
#1145=EDGE_CURVE ( 'NONE', #20782, #4317, #9888, .T. ) ;
#1157=VERTEX_POINT ( 'NONE', #15962 ) ;
#1191=CARTESIAN_POINT ( 'NONE',  ( 0.2500000000000002220, 0.000000000000000000, 0.000000000000000000 ) ) ;
#1264=CARTESIAN_POINT ( 'NONE',  ( 0.000000000000000000, 5.051668046482832750E-16, -4.000000000000000000 ) ) ;
#1306=PLANE ( 'NONE',  #17938 ) ;
#1325=VECTOR ( 'NONE', #16725, 999.9999999999997726 ) ;
#1334=EDGE_LOOP ( 'NONE', ( #13815, #13963, #11908, #18201, #9704 ) ) ;
#1349=LINE ( 'NONE', #17789, #15417 ) ;
#1355=CARTESIAN_POINT ( 'NONE',  ( 0.000000000000000000, -1.178949249685214307, 2.042000000000001592 ) ) ;
#1409=CARTESIAN_POINT ( 'NONE',  ( 5.000000000000000888, 0.000000000000000000, 0.000000000000000000 ) ) ;
#1413=AXIS2_PLACEMENT_3D ( 'NONE', #8127, #13816, #19200 ) ;
#1428=EDGE_LOOP ( 'NONE', ( #4910, #5715, #19219 ) ) ;
#1483=CARTESIAN_POINT ( 'NONE',  ( 2.500000000000000000, 0.000000000000000000, 0.000000000000000000 ) ) ;
#1548=DIRECTION ( 'NONE',  ( 1.000000000000000000, 0.000000000000000000, 0.000000000000000000 ) ) ;
#1557=ADVANCED_FACE ( 'NONE', ( #22917 ), #1306, .F. ) ;
#1618=ADVANCED_FACE ( 'NONE', ( #7343, #14725 ), #23537, .T. ) ;
#1682=ORIENTED_EDGE ( 'NONE', *, *, #17229, .T. ) ;
#1742=CIRCLE ( 'NONE', #21820, 4.250000000000000000 ) ;
#1754=VERTEX_POINT ( 'NONE', #14958 ) ;
#1756=DIRECTION ( 'NONE',  ( 0.000000000000000000, 0.000000000000000000, -1.000000000000000000 ) ) ;
#1782=PLANE ( 'NONE',  #6580 ) ;
#1819=DIRECTION ( 'NONE',  ( 0.000000000000000000, 1.000000000000000000, -1.287488025362403787E-15 ) ) ;
#1829=CIRCLE ( 'NONE', #15362, 4.250000000000000000 ) ;
#1834=CARTESIAN_POINT ( 'NONE',  ( 2.500000000000000000, -1.768423874527825568, -1.020999999999998575 ) ) ;
#1840=EDGE_LOOP ( 'NONE', ( #23285, #20964 ) ) ;
#1890=DIRECTION ( 'NONE',  ( -1.000000000000000000, 0.000000000000000000, -0.000000000000000000 ) ) ;
#1902=DIRECTION ( 'NONE',  ( 0.000000000000000000, 0.5000000000000011102, 0.8660254037844379305 ) ) ;
#1920=DIRECTION ( 'NONE',  ( 0.000000000000000000, 0.000000000000000000, 1.000000000000000000 ) ) ;
#1961=ORIENTED_EDGE ( 'NONE', *, *, #21494, .T. ) ;
#1982=CARTESIAN_POINT ( 'NONE',  ( 2.500000000000000000, 2.357898499370431722, -2.818925648462311528E-15 ) ) ;
#2059=AXIS2_PLACEMENT_3D ( 'NONE', #3328, #21587, #21697 ) ;
#2086=( NAMED_UNIT ( * ) SI_UNIT ( $, .STERADIAN. ) SOLID_ANGLE_UNIT ( ) );
#2108=CARTESIAN_POINT ( 'NONE',  ( 2.500000000000000000, 2.500728763858895382E-16, -2.041999999999999815 ) ) ;
#2170=EDGE_CURVE ( 'NONE', #19782, #15625, #13019, .T. ) ;
#2176=ORIENTED_EDGE ( 'NONE', *, *, #14759, .T. ) ;
#2181=DIRECTION ( 'NONE',  ( 0.000000000000000000, -0.4999999999999993339, 0.8660254037844390407 ) ) ;
#2219=ORIENTED_EDGE ( 'NONE', *, *, #1073, .T. ) ;
#2237=ORIENTED_EDGE ( 'NONE', *, *, #9220, .T. ) ;
#2289=ORIENTED_EDGE ( 'NONE', *, *, #7190, .T. ) ;
#2293=CARTESIAN_POINT ( 'NONE',  ( 3.678949249685231848, 0.000000000000000000, 0.000000000000000000 ) ) ;
#2357=DIRECTION ( 'NONE',  ( 0.000000000000000000, -0.5000000000000009992, -0.8660254037844380415 ) ) ;
#2358=EDGE_CURVE ( 'NONE', #18246, #16847, #12060, .T. ) ;
#2407=DIRECTION ( 'NONE',  ( 0.000000000000000000, -0.5000000000000013323, -0.8660254037844380415 ) ) ;
#2434=ORIENTED_EDGE ( 'NONE', *, *, #21712, .F. ) ;
#2440=CARTESIAN_POINT ( 'NONE',  ( 5.000000000000000888, 0.000000000000000000, 0.000000000000000000 ) ) ;
#2495=DIRECTION ( 'NONE',  ( 1.000000000000000000, 0.000000000000000000, 0.000000000000000000 ) ) ;
#2527=ORIENTED_EDGE ( 'NONE', *, *, #15560, .F. ) ;
#2540=AXIS2_PLACEMENT_3D ( 'NONE', #3175, #6811, #5010 ) ;
#2551=EDGE_CURVE ( 'NONE', #3909, #16080, #4116, .T. ) ;
#2608=PLANE ( 'NONE',  #19356 ) ;
#2617=AXIS2_PLACEMENT_3D ( 'NONE', #196, #7549, #20468 ) ;
#2695=CARTESIAN_POINT ( 'NONE',  ( 2.500000000000000000, -2.357898499370432166, 3.035766082959412415E-15 ) ) ;
#2711=DIRECTION ( 'NONE',  ( 0.000000000000000000, 0.000000000000000000, 1.000000000000000000 ) ) ;
#2733=LINE ( 'NONE', #4774, #13446 ) ;
#2737=CARTESIAN_POINT ( 'NONE',  ( 5.200000000000002842, 0.000000000000000000, 0.000000000000000000 ) ) ;
#2799=ORIENTED_EDGE ( 'NONE', *, *, #863, .T. ) ;
#3074=DIRECTION ( 'NONE',  ( 0.000000000000000000, 0.000000000000000000, 1.000000000000000000 ) ) ;
#3162=DIRECTION ( 'NONE',  ( 0.000000000000000000, -1.000000000000000000, 1.287488025362403787E-15 ) ) ;
#3175=CARTESIAN_POINT ( 'NONE',  ( -31.74999999999995737, 0.000000000000000000, 0.000000000000000000 ) ) ;
#3283=AXIS2_PLACEMENT_3D ( 'NONE', #10073, #12028, #13954 ) ;
#3293=CARTESIAN_POINT ( 'NONE',  ( 20.55500000000001748, 0.000000000000000000, 0.000000000000000000 ) ) ;
#3328=CARTESIAN_POINT ( 'NONE',  ( 20.55500000000001748, 0.000000000000000000, 0.000000000000000000 ) ) ;
#3369=AXIS2_PLACEMENT_3D ( 'NONE', #12581, #1548, #8933 ) ;
#3424=VECTOR ( 'NONE', #14180, 1000.000000000000114 ) ;
#3430=DIRECTION ( 'NONE',  ( 0.000000000000000000, 0.000000000000000000, -1.000000000000000000 ) ) ;
#3431=DIRECTION ( 'NONE',  ( -1.000000000000000000, -0.000000000000000000, -0.000000000000000000 ) ) ;
#3456=DIRECTION ( 'NONE',  ( 0.000000000000000000, 0.000000000000000000, -1.000000000000000000 ) ) ;
#3566=ORIENTED_EDGE ( 'NONE', *, *, #20563, .F. ) ;
#3583=ORIENTED_EDGE ( 'NONE', *, *, #21673, .F. ) ;
#3617=EDGE_CURVE ( 'NONE', #12251, #16080, #14698, .T. ) ;
#3628=ADVANCED_FACE ( 'NONE', ( #5731 ), #11077, .T. ) ;
#3630=VERTEX_POINT ( 'NONE', #72 ) ;
#3701=ADVANCED_FACE ( 'NONE', ( #15054 ), #16582, .T. ) ;
#3720=DIRECTION ( 'NONE',  ( -1.000000000000000000, -0.000000000000000000, -0.000000000000000000 ) ) ;
#3743=CIRCLE ( 'NONE', #17628, 0.2000000000000000944 ) ;
#3769=DIRECTION ( 'NONE',  ( 1.000000000000000000, 0.000000000000000000, 0.000000000000000000 ) ) ;
#3788=DIRECTION ( 'NONE',  ( -1.000000000000000000, -0.000000000000000000, -0.000000000000000000 ) ) ;
#3814=VECTOR ( 'NONE', #2181, 1000.000000000000000 ) ;
#3872=EDGE_CURVE ( 'NONE', #19527, #20235, #6195, .T. ) ;
#3884=ADVANCED_FACE ( 'NONE', ( #16345 ), #4992, .F. ) ;
#3887=CARTESIAN_POINT ( 'NONE',  ( 5.200000000000002842, 0.000000000000000000, 0.000000000000000000 ) ) ;
#3909=VERTEX_POINT ( 'NONE', #18258 ) ;
#3985=VERTEX_POINT ( 'NONE', #21769 ) ;
#4116=LINE ( 'NONE', #11526, #3814 ) ;
#4152=DIRECTION ( 'NONE',  ( 0.000000000000000000, 0.000000000000000000, -1.000000000000000000 ) ) ;
#4188=DIRECTION ( 'NONE',  ( -1.000000000000000000, -0.000000000000000000, -0.000000000000000000 ) ) ;
#4209=DIRECTION ( 'NONE',  ( 1.000000000000000000, 0.000000000000000000, 0.000000000000000000 ) ) ;
#4212=EDGE_LOOP ( 'NONE', ( #7732, #11570, #10090, #10515, #5353 ) ) ;
#4255=EDGE_CURVE ( 'NONE', #18246, #12251, #18233, .T. ) ;
#4278=DIRECTION ( 'NONE',  ( -1.000000000000000000, -0.000000000000000000, -0.000000000000000000 ) ) ;
#4304=ORIENTED_EDGE ( 'NONE', *, *, #22470, .T. ) ;
#4317=VERTEX_POINT ( 'NONE', #14518 ) ;
#4383=VECTOR ( 'NONE', #11332, 1000.000000000000114 ) ;
#4393=CARTESIAN_POINT ( 'NONE',  ( 2.500000000000000000, -1.178949249685214307, 2.042000000000001592 ) ) ;
#4412=CARTESIAN_POINT ( 'NONE',  ( 0.000000000000000000, 0.000000000000000000, 0.000000000000000000 ) ) ;
#4428=EDGE_CURVE ( 'NONE', #12251, #3909, #10629, .T. ) ;
#4460=EDGE_CURVE ( 'NONE', #18754, #14046, #22163, .T. ) ;
#4505=EDGE_LOOP ( 'NONE', ( #8779, #12804, #18791 ) ) ;
#4577=DIRECTION ( 'NONE',  ( 0.000000000000000000, 0.000000000000000000, -1.000000000000000000 ) ) ;
#4604=VECTOR ( 'NONE', #22600, 1000.000000000000114 ) ;
#4623=MECHANICAL_DESIGN_GEOMETRIC_PRESENTATION_REPRESENTATION('',(#6554),#18861);
#4632=ORIENTED_EDGE ( 'NONE', *, *, #13014, .F. ) ;
#4664=MANIFOLD_SOLID_BREP ( 'Hex', #18690 ) ;
#4774=CARTESIAN_POINT ( 'NONE',  ( 21.00000000000000355, 0.000000000000000000, 2.055000000000000160 ) ) ;
#4831=ORIENTED_EDGE ( 'NONE', *, *, #19298, .F. ) ;
#4910=ORIENTED_EDGE ( 'NONE', *, *, #23370, .F. ) ;
#4914=ORIENTED_EDGE ( 'NONE', *, *, #10968, .F. ) ;
#4931=ADVANCED_FACE ( 'NONE', ( #6694 ), #19724, .T. ) ;
#4942=ORIENTED_EDGE ( 'NONE', *, *, #18044, .F. ) ;
#4952=DIRECTION ( 'NONE',  ( 0.000000000000000000, 0.000000000000000000, 1.000000000000000000 ) ) ;
#4974=DIRECTION ( 'NONE',  ( 1.000000000000000000, 0.000000000000000000, 0.000000000000000000 ) ) ;
#4992=CONICAL_SURFACE ( 'NONE', #17707, 2.041999999999999815, 1.047197551196591858 ) ;
#5010=DIRECTION ( 'NONE',  ( 0.000000000000000000, 0.000000000000000000, 1.000000000000000000 ) ) ;
#5035=CARTESIAN_POINT ( 'NONE',  ( 0.000000000000000000, 1.178949249685212974, -2.042000000000001148 ) ) ;
#5089=DIRECTION ( 'NONE',  ( 0.000000000000000000, 0.000000000000000000, -1.000000000000000000 ) ) ;
#5150=AXIS2_PLACEMENT_3D ( 'NONE', #19484, #21427, #3074 ) ;
#5169=PLANE ( 'NONE',  #3369 ) ;
#5208=EDGE_LOOP ( 'NONE', ( #20286, #13243, #23748 ) ) ;
#5223=LINE ( 'NONE', #1355, #14298 ) ;
#5257=DIRECTION ( 'NONE',  ( 0.000000000000000000, -1.000000000000000000, 1.287488025362403787E-15 ) ) ;
#5321=ORIENTED_EDGE ( 'NONE', *, *, #3617, .T. ) ;
#5333=ORIENTED_EDGE ( 'NONE', *, *, #3872, .T. ) ;
#5353=ORIENTED_EDGE ( 'NONE', *, *, #2358, .T. ) ;
#5362=ADVANCED_FACE ( 'NONE', ( #8353 ), #23199, .T. ) ;
#5395=DIRECTION ( 'NONE',  ( 0.000000000000000000, -1.000000000000000000, 0.000000000000000000 ) ) ;
#5412=CIRCLE ( 'NONE', #23135, 2.041999999999999815 ) ;
#5494=DIRECTION ( 'NONE',  ( 0.000000000000000000, 1.000000000000000000, -1.287488025362403787E-15 ) ) ;
#5547=CARTESIAN_POINT ( 'NONE',  ( 2.500000000000000000, 0.000000000000000000, 0.000000000000000000 ) ) ;
#5613=DIRECTION ( 'NONE',  ( 0.000000000000000000, 0.000000000000000000, 1.000000000000000000 ) ) ;
#5615=( NAMED_UNIT ( * ) SI_UNIT ( $, .STERADIAN. ) SOLID_ANGLE_UNIT ( ) );
#5641=AXIS2_PLACEMENT_3D ( 'NONE', #17200, #4278, #11431 ) ;
#5669=VERTEX_POINT ( 'NONE', #2293 ) ;
#5715=ORIENTED_EDGE ( 'NONE', *, *, #2170, .T. ) ;
#5731=FACE_OUTER_BOUND ( 'NONE', #18854, .T. ) ;
#5854=DIRECTION ( 'NONE',  ( 1.000000000000000000, 0.000000000000000000, 0.000000000000000000 ) ) ;
#5899=DIRECTION ( 'NONE',  ( -1.000000000000000000, -0.000000000000000000, -0.000000000000000000 ) ) ;
#5918=DIRECTION ( 'NONE',  ( -0.5000000000000051070, 0.000000000000000000, 0.8660254037844355990 ) ) ;
#5921=ADVANCED_FACE ( 'NONE', ( #18329 ), #1782, .F. ) ;
#5948=DIRECTION ( 'NONE',  ( -1.000000000000000000, -0.000000000000000000, -0.000000000000000000 ) ) ;
#6119=LINE ( 'NONE', #22417, #7115 ) ;
#6135=APPLICATION_CONTEXT ( 'automotive_design' ) ;
#6160=AXIS2_PLACEMENT_3D ( 'NONE', #21050, #15746, #8504 ) ;
#6172=CARTESIAN_POINT ( 'NONE',  ( 21.00000000000000355, 0.000000000000000000, 2.055000000000000160 ) ) ;
#6177=PRODUCT_DEFINITION_FORMATION_WITH_SPECIFIED_SOURCE ( 'ANY', '', #20194, .NOT_KNOWN. ) ;
#6195=CIRCLE ( 'NONE', #15817, 2.500000000000000444 ) ;
#6204=ADVANCED_FACE ( 'NONE', ( #8553 ), #8308, .F. ) ;
#6221=PLANE ( 'NONE',  #16339 ) ;
#6236=SHAPE_REPRESENTATION ( 'socket head cap screw_iso_ISO 4762 M5 x 16 - 16N', ( #11210 ), #9660 ) ;
#6242=ORIENTED_EDGE ( 'NONE', *, *, #4428, .F. ) ;
#6309=LINE ( 'NONE', #2695, #3424 ) ;
#6323=DIRECTION ( 'NONE',  ( -1.000000000000000000, -0.000000000000000000, -0.000000000000000000 ) ) ;
#6435=CARTESIAN_POINT ( 'NONE',  ( 0.2500000000000002220, 0.000000000000000000, 0.000000000000000000 ) ) ;
#6441=CIRCLE ( 'NONE', #21862, 2.041999999999999815 ) ;
#6451=VERTEX_POINT ( 'NONE', #11223 ) ;
#6493=EDGE_CURVE ( 'NONE', #18246, #6451, #22633, .T. ) ;
#6543=FACE_OUTER_BOUND ( 'NONE', #13817, .T. ) ;
#6554=STYLED_ITEM ( 'NONE', ( #16607 ), #15670 ) ;
#6580=AXIS2_PLACEMENT_3D ( 'NONE', #801, #18112, #1902 ) ;
#6584=DIRECTION ( 'NONE',  ( -0.000000000000000000, 0.8660254037844392627, 0.4999999999999990008 ) ) ;
#6608=DIRECTION ( 'NONE',  ( -1.000000000000000000, -0.000000000000000000, -0.000000000000000000 ) ) ;
#6694=FACE_OUTER_BOUND ( 'NONE', #23503, .T. ) ;
#6695=ORIENTED_EDGE ( 'NONE', *, *, #12887, .F. ) ;
#6796=CARTESIAN_POINT ( 'NONE',  ( 2.500000000000000000, 1.178949249685212974, -2.042000000000001148 ) ) ;
#6811=DIRECTION ( 'NONE',  ( -1.000000000000000000, -0.000000000000000000, -0.000000000000000000 ) ) ;
#6888=CARTESIAN_POINT ( 'NONE',  ( 0.2500000000000002220, 0.000000000000000000, 4.000000000000000000 ) ) ;
#6895=VECTOR ( 'NONE', #6323, 1000.000000000000000 ) ;
#6934=COLOUR_RGB ( '',1.000000000000000000, 0.9490196078431372140, 0.9098039215686274384 ) ;
#6935=AXIS2_PLACEMENT_3D ( 'NONE', #17335, #6584, #785 ) ;
#6956=DIRECTION ( 'NONE',  ( 1.000000000000000000, 0.000000000000000000, 0.000000000000000000 ) ) ;
#6991=EDGE_LOOP ( 'NONE', ( #9027, #7737, #9844, #23326 ) ) ;
#7010=CARTESIAN_POINT ( 'NONE',  ( 0.2500000000000002220, 4.898587196589412829E-16, -4.000000000000000000 ) ) ;
#7012=ADVANCED_FACE ( 'NONE', ( #9650 ), #2608, .F. ) ;
#7077=PLANE ( 'NONE',  #17749 ) ;
#7115=VECTOR ( 'NONE', #13049, 1000.000000000000000 ) ;
#7150=VECTOR ( 'NONE', #16082, 1000.000000000000000 ) ;
#7166=( NAMED_UNIT ( * ) SI_UNIT ( $, .STERADIAN. ) SOLID_ANGLE_UNIT ( ) );
#7184=CARTESIAN_POINT ( 'NONE',  ( 2.500000000000000000, -1.178949249685214307, 2.042000000000001592 ) ) ;
#7188=CARTESIAN_POINT ( 'NONE',  ( 0.000000000000000000, -1.178949249685218748, -2.041999999999998039 ) ) ;
#7190=EDGE_CURVE ( 'NONE', #14046, #18754, #7826, .T. ) ;
#7268=ORIENTED_EDGE ( 'NONE', *, *, #21842, .F. ) ;
#7297=FACE_OUTER_BOUND ( 'NONE', #40, .T. ) ;
#7343=FACE_BOUND ( 'NONE', #21964, .T. ) ;
#7357=PRODUCT_CONTEXT ( 'NONE', #6135, 'mechanical' ) ;
#7364=UNCERTAINTY_MEASURE_WITH_UNIT (LENGTH_MEASURE( 1.000000000000000082E-05 ), #18518, 'distance_accuracy_value', 'NONE');
#7365=APPLICATION_CONTEXT ( 'automotive_design' ) ;
#7366=LINE ( 'NONE', #16424, #22164 ) ;
#7401=ORIENTED_EDGE ( 'NONE', *, *, #13896, .T. ) ;
#7414=EDGE_LOOP ( 'NONE', ( #10826, #14587 ) ) ;
#7433=CARTESIAN_POINT ( 'NONE',  ( 5.200000000000002842, 0.000000000000000000, -2.700000000000000622 ) ) ;
#7438=DIRECTION ( 'NONE',  ( 0.000000000000000000, 0.000000000000000000, -1.000000000000000000 ) ) ;
#7526=VECTOR ( 'NONE', #5899, 1000.000000000000000 ) ;
#7549=DIRECTION ( 'NONE',  ( -1.000000000000000000, -0.000000000000000000, -0.000000000000000000 ) ) ;
#7554=DIRECTION ( 'NONE',  ( 0.000000000000000000, 0.4999999999999990008, -0.8660254037844391517 ) ) ;
#7617=EDGE_CURVE ( 'NONE', #711, #20235, #23156, .T. ) ;
#7641=DIRECTION ( 'NONE',  ( 0.000000000000000000, 0.000000000000000000, -1.000000000000000000 ) ) ;
#7696=AXIS2_PLACEMENT_3D ( 'NONE', #21705, #14831, #1756 ) ;
#7704=ORIENTED_EDGE ( 'NONE', *, *, #22227, .F. ) ;
#7723=EDGE_LOOP ( 'NONE', ( #15081, #18971, #8325, #22334 ) ) ;
#7732=ORIENTED_EDGE ( 'NONE', *, *, #9789, .T. ) ;
#7737=ORIENTED_EDGE ( 'NONE', *, *, #7617, .T. ) ;
#7776=SURFACE_SIDE_STYLE ('',( #10951 ) ) ;
#7787=CARTESIAN_POINT ( 'NONE',  ( 2.500000000000000000, 2.357898499370431722, -2.818925648462311528E-15 ) ) ;
#7791=ORIENTED_EDGE ( 'NONE', *, *, #863, .F. ) ;
#7796=EDGE_CURVE ( 'NONE', #14436, #3630, #881, .T. ) ;
#7809=EDGE_LOOP ( 'NONE', ( #19533, #17662, #23628, #13671 ) ) ;
#7826=CIRCLE ( 'NONE', #20933, 2.055000000000000160 ) ;
#7858=CARTESIAN_POINT ( 'NONE',  ( 2.500000000000000000, 1.178949249685212974, -2.042000000000001148 ) ) ;
#7880=VERTEX_POINT ( 'NONE', #13169 ) ;
#7959=CARTESIAN_POINT ( 'NONE',  ( 2.500000000000000000, 2.357898499370431722, -2.818925648462311528E-15 ) ) ;
#7967=DIRECTION ( 'NONE',  ( 0.000000000000000000, 0.000000000000000000, 1.000000000000000000 ) ) ;
#7996=EDGE_CURVE ( 'NONE', #4317, #8057, #16327, .T. ) ;
#8004=EDGE_CURVE ( 'NONE', #6451, #12251, #10571, .T. ) ;
#8019=AXIS2_PLACEMENT_3D ( 'NONE', #8897, #18004, #3430 ) ;
#8024=CIRCLE ( 'NONE', #2617, 4.000000000000000000 ) ;
#8052=ADVANCED_FACE ( 'NONE', ( #21316 ), #12182, .T. ) ;
#8057=VERTEX_POINT ( 'NONE', #1264 ) ;
#8113=DIRECTION ( 'NONE',  ( 0.000000000000000000, 0.000000000000000000, 1.000000000000000000 ) ) ;
#8127=CARTESIAN_POINT ( 'NONE',  ( 2.500000000000000000, 1.178949249685212974, -2.042000000000001148 ) ) ;
#8174=DIRECTION ( 'NONE',  ( 0.000000000000000000, -0.5000000000000009992, -0.8660254037844380415 ) ) ;
#8205=ORIENTED_EDGE ( 'NONE', *, *, #13014, .T. ) ;
#8248=ORIENTED_EDGE ( 'NONE', *, *, #23370, .T. ) ;
#8286=ORIENTED_EDGE ( 'NONE', *, *, #9789, .F. ) ;
#8308=PLANE ( 'NONE',  #14314 ) ;
#8325=ORIENTED_EDGE ( 'NONE', *, *, #22785, .F. ) ;
#8353=FACE_OUTER_BOUND ( 'NONE', #19074, .T. ) ;
#8387=DIRECTION ( 'NONE',  ( -1.000000000000000000, -0.000000000000000000, -0.000000000000000000 ) ) ;
#8390=DIRECTION ( 'NONE',  ( -1.000000000000000000, -0.000000000000000000, -0.000000000000000000 ) ) ;
#8420=CIRCLE ( 'NONE', #14600, 0.2000000000000000944 ) ;
#8425=DIRECTION ( 'NONE',  ( 1.000000000000000000, 0.000000000000000000, 0.000000000000000000 ) ) ;
#8447=EDGE_CURVE ( 'NONE', #9681, #8057, #9143, .T. ) ;
#8504=DIRECTION ( 'NONE',  ( 0.000000000000000000, 0.000000000000000000, 1.000000000000000000 ) ) ;
#8553=FACE_OUTER_BOUND ( 'NONE', #18562, .T. ) ;
#8613=CARTESIAN_POINT ( 'NONE',  ( 2.500000000000000000, 1.768423874527822459, -1.021000000000002794 ) ) ;
#8668=DIRECTION ( 'NONE',  ( -1.000000000000000000, -0.000000000000000000, -0.000000000000000000 ) ) ;
#8678=EDGE_CURVE ( 'NONE', #20782, #9681, #1057, .T. ) ;
#8710=LINE ( 'NONE', #10662, #21848 ) ;
#8779=ORIENTED_EDGE ( 'NONE', *, *, #6493, .F. ) ;
#8793=AXIS2_PLACEMENT_3D ( 'NONE', #10202, #15884, #14195 ) ;
#8829=DIRECTION ( 'NONE',  ( -0.7071067811865364705, 8.659560562355067211E-17, -0.7071067811865584529 ) ) ;
#8831=CARTESIAN_POINT ( 'NONE',  ( 2.500000000000000000, 1.178949249685212974, -2.042000000000001148 ) ) ;
#8897=CARTESIAN_POINT ( 'NONE',  ( 2.500000000000000000, 2.357898499370431722, -2.818925648462311528E-15 ) ) ;
#8933=DIRECTION ( 'NONE',  ( 0.000000000000000000, 0.000000000000000000, -1.000000000000000000 ) ) ;
#9027=ORIENTED_EDGE ( 'NONE', *, *, #19170, .T. ) ;
#9028=ORIENTED_EDGE ( 'NONE', *, *, #14228, .T. ) ;
#9031=FACE_OUTER_BOUND ( 'NONE', #7723, .T. ) ;
#9067=VECTOR ( 'NONE', #20272, 1000.000000000000000 ) ;
#9142=LINE ( 'NONE', #22046, #15793 ) ;
#9143=CIRCLE ( 'NONE', #22617, 0.2500000000000002220 ) ;
#9163=DIRECTION ( 'NONE',  ( 0.000000000000000000, -0.5000000000000013323, -0.8660254037844380415 ) ) ;
#9169=ORIENTED_EDGE ( 'NONE', *, *, #17022, .F. ) ;
#9181=CIRCLE ( 'NONE', #18411, 2.500000000000000444 ) ;
#9191=ORIENTED_EDGE ( 'NONE', *, *, #15560, .T. ) ;
#9209=EDGE_LOOP ( 'NONE', ( #23694, #15652, #1961, #13588, #16092 ) ) ;
#9220=EDGE_CURVE ( 'NONE', #14046, #3985, #2733, .T. ) ;
#9235=PRODUCT_DEFINITION_SHAPE ( 'NONE', 'NONE',  #1042 ) ;
#9241=TOROIDAL_SURFACE ( 'NONE', #18473, 4.000000000000000000, 0.2500000000000000000 ) ;
#9260=AXIS2_PLACEMENT_3D ( 'NONE', #1982, #18628, #14810 ) ;
#9328=ADVANCED_FACE ( 'NONE', ( #7297 ), #18387, .F. ) ;
#9473=CARTESIAN_POINT ( 'NONE',  ( 0.000000000000000000, 0.000000000000000000, 0.000000000000000000 ) ) ;
#9542=CARTESIAN_POINT ( 'NONE',  ( 21.00000000000000355, 0.000000000000000000, 0.000000000000000000 ) ) ;
#9650=FACE_OUTER_BOUND ( 'NONE', #19725, .T. ) ;
#9660=( GEOMETRIC_REPRESENTATION_CONTEXT ( 3 ) GLOBAL_UNCERTAINTY_ASSIGNED_CONTEXT ( ( #15109 ) ) GLOBAL_UNIT_ASSIGNED_CONTEXT ( ( #10843, #19735, #7166 ) ) REPRESENTATION_CONTEXT ( 'NONE', 'WORKASPACE' ) );
#9674=PLANE ( 'NONE',  #23345 ) ;
#9681=VERTEX_POINT ( 'NONE', #14319 ) ;
#9704=ORIENTED_EDGE ( 'NONE', *, *, #522, .T. ) ;
#9755=CARTESIAN_POINT ( 'NONE',  ( 2.500000000000000000, 1.178949249685217415, 2.041999999999998483 ) ) ;
#9789=EDGE_CURVE ( 'NONE', #16847, #19722, #5223, .T. ) ;
#9790=DIRECTION ( 'NONE',  ( -1.000000000000000000, -0.000000000000000000, -0.000000000000000000 ) ) ;
#9844=ORIENTED_EDGE ( 'NONE', *, *, #18044, .T. ) ;
#9847=AXIS2_PLACEMENT_3D ( 'NONE', #12937, #1890, #12829 ) ;
#9888=CIRCLE ( 'NONE', #22191, 0.2500000000000002220 ) ;
#9904=DIRECTION ( 'NONE',  ( 1.000000000000000000, 0.000000000000000000, 0.000000000000000000 ) ) ;
#9932=DIRECTION ( 'NONE',  ( 0.000000000000000000, 0.000000000000000000, 1.000000000000000000 ) ) ;
#9984=CARTESIAN_POINT ( 'NONE',  ( 2.500000000000000000, -1.178949249685214307, 2.042000000000001592 ) ) ;
#10019=ADVANCED_FACE ( 'NONE', ( #11765 ), #13884, .T. ) ;
#10028=CARTESIAN_POINT ( 'NONE',  ( 0.2500000000000002220, 0.000000000000000000, 0.000000000000000000 ) ) ;
#10046=AXIS2_PLACEMENT_3D ( 'NONE', #3293, #18349, #16676 ) ;
#10073=CARTESIAN_POINT ( 'NONE',  ( 21.00000000000000355, 0.000000000000000000, 0.000000000000000000 ) ) ;
#10090=ORIENTED_EDGE ( 'NONE', *, *, #3617, .F. ) ;
#10118=DIRECTION ( 'NONE',  ( -0.7071067811865364705, 0.000000000000000000, 0.7071067811865584529 ) ) ;
#10202=CARTESIAN_POINT ( 'NONE',  ( 2.500000000000000000, -1.178949249685214307, 2.042000000000001592 ) ) ;
#10222=DIRECTION ( 'NONE',  ( -1.000000000000000000, -0.000000000000000000, -0.000000000000000000 ) ) ;
#10292=LINE ( 'NONE', #8831, #7150 ) ;
#10361=ADVANCED_FACE ( 'NONE', ( #23490 ), #779, .F. ) ;
#10368=CIRCLE ( 'NONE', #16912, 2.700000000000000622 ) ;
#10388=CIRCLE ( 'NONE', #14615, 2.041999999999999815 ) ;
#10456=FACE_OUTER_BOUND ( 'NONE', #15148, .T. ) ;
#10487=DIRECTION ( 'NONE',  ( 0.000000000000000000, 0.000000000000000000, -1.000000000000000000 ) ) ;
#10515=ORIENTED_EDGE ( 'NONE', *, *, #4255, .F. ) ;
#10523=EDGE_LOOP ( 'NONE', ( #16756, #12360 ) ) ;
#10571=CIRCLE ( 'NONE', #132, 2.041999999999999815 ) ;
#10598=ORIENTED_EDGE ( 'NONE', *, *, #10682, .F. ) ;
#10629=CIRCLE ( 'NONE', #19850, 2.041999999999999815 ) ;
#10662=CARTESIAN_POINT ( 'NONE',  ( 21.00000000000000355, 2.516649172247811061E-16, -2.055000000000000160 ) ) ;
#10671=DIRECTION ( 'NONE',  ( 0.000000000000000000, 0.000000000000000000, -1.000000000000000000 ) ) ;
#10682=EDGE_CURVE ( 'NONE', #21824, #12819, #15988, .T. ) ;
#10778=ADVANCED_FACE ( 'NONE', ( #10456 ), #15633, .T. ) ;
#10820=ADVANCED_FACE ( 'NONE', ( #12158 ), #9241, .T. ) ;
#10826=ORIENTED_EDGE ( 'NONE', *, *, #7996, .T. ) ;
#10843=( LENGTH_UNIT ( ) NAMED_UNIT ( * ) SI_UNIT ( .MILLI., .METRE. ) );
#10866=FACE_OUTER_BOUND ( 'NONE', #4212, .T. ) ;
#10890=LINE ( 'NONE', #11246, #13061 ) ;
#10923=VERTEX_POINT ( 'NONE', #22927 ) ;
#10951=SURFACE_STYLE_FILL_AREA ( #13009 ) ;
#10968=EDGE_CURVE ( 'NONE', #9681, #20782, #15623, .T. ) ;
#10978=CARTESIAN_POINT ( 'NONE',  ( 2.500000000000000000, 0.000000000000000000, 0.000000000000000000 ) ) ;
#11037=AXIS2_PLACEMENT_3D ( 'NONE', #9542, #9790, #7967 ) ;
#11051=DIRECTION ( 'NONE',  ( -1.000000000000000000, -0.000000000000000000, -0.000000000000000000 ) ) ;
#11077=PLANE ( 'NONE',  #9260 ) ;
#11103=ADVANCED_FACE ( 'NONE', ( #20691 ), #6221, .F. ) ;
#11210=AXIS2_PLACEMENT_3D ( 'NONE', #9473, #14914, #3769 ) ;
#11223=CARTESIAN_POINT ( 'NONE',  ( 2.500000000000000000, -1.768423874527823569, 1.021000000000002350 ) ) ;
#11246=CARTESIAN_POINT ( 'NONE',  ( 0.000000000000000000, 2.357898499370431722, -2.818925648462311528E-15 ) ) ;
#11296=DIRECTION ( 'NONE',  ( 1.000000000000000000, 0.000000000000000000, 0.000000000000000000 ) ) ;
#11332=DIRECTION ( 'NONE',  ( -0.5000000000000051070, 1.060575238724903217E-16, -0.8660254037844355990 ) ) ;
#11386=LINE ( 'NONE', #22571, #704 ) ;
#11431=DIRECTION ( 'NONE',  ( 0.000000000000000000, 0.000000000000000000, 1.000000000000000000 ) ) ;
#11526=CARTESIAN_POINT ( 'NONE',  ( 2.500000000000000000, 2.357898499370431722, -2.818925648462311528E-15 ) ) ;
#11535=LINE ( 'NONE', #15267, #4604 ) ;
#11570=ORIENTED_EDGE ( 'NONE', *, *, #14228, .F. ) ;
#11597=VECTOR ( 'NONE', #12273, 1000.000000000000000 ) ;
#11681=CYLINDRICAL_SURFACE ( 'NONE', #5641, 4.250000000000000000 ) ;
#11692=DIRECTION ( 'NONE',  ( 0.000000000000000000, 0.000000000000000000, 1.000000000000000000 ) ) ;
#11735=UNCERTAINTY_MEASURE_WITH_UNIT (LENGTH_MEASURE( 1.000000000000000082E-05 ), #18533, 'distance_accuracy_value', 'NONE');
#11765=FACE_OUTER_BOUND ( 'NONE', #23126, .T. ) ;
#11802=DIRECTION ( 'NONE',  ( -1.000000000000000000, -0.000000000000000000, -0.000000000000000000 ) ) ;
#11831=MECHANICAL_DESIGN_GEOMETRIC_PRESENTATION_REPRESENTATION('',(#15268),#962);
#11841=CARTESIAN_POINT ( 'NONE',  ( 2.500000000000000000, 0.000000000000000000, 0.000000000000000000 ) ) ;
#11908=ORIENTED_EDGE ( 'NONE', *, *, #6493, .T. ) ;
#11912=EDGE_LOOP ( 'NONE', ( #792, #2434, #4831, #13660, #20777 ) ) ;
#11961=AXIS2_PLACEMENT_3D ( 'NONE', #2737, #6956, #10487 ) ;
#11967=VECTOR ( 'NONE', #4188, 1000.000000000000000 ) ;
#11980=CARTESIAN_POINT ( 'NONE',  ( -31.74999999999995737, 3.061616997868383634E-16, -2.500000000000000444 ) ) ;
#12028=DIRECTION ( 'NONE',  ( -1.000000000000000000, -0.000000000000000000, -0.000000000000000000 ) ) ;
#12048=ORIENTED_EDGE ( 'NONE', *, *, #4428, .T. ) ;
#12060=LINE ( 'NONE', #4393, #6895 ) ;
#12143=DIRECTION ( 'NONE',  ( -1.000000000000000000, -0.000000000000000000, -0.000000000000000000 ) ) ;
#12158=FACE_OUTER_BOUND ( 'NONE', #22805, .T. ) ;
#12161=FACE_OUTER_BOUND ( 'NONE', #1334, .T. ) ;
#12182=CYLINDRICAL_SURFACE ( 'NONE', #5150, 2.500000000000000444 ) ;
#12251=VERTEX_POINT ( 'NONE', #18534 ) ;
#12273=DIRECTION ( 'NONE',  ( -1.000000000000000000, -0.000000000000000000, -0.000000000000000000 ) ) ;
#12360=ORIENTED_EDGE ( 'NONE', *, *, #7796, .T. ) ;
#12384=VECTOR ( 'NONE', #2407, 999.9999999999997726 ) ;
#12455=VERTEX_POINT ( 'NONE', #1834 ) ;
#12456=CARTESIAN_POINT ( 'NONE',  ( 0.000000000000000000, 1.178949249685217415, 2.041999999999998483 ) ) ;
#12511=LINE ( 'NONE', #19821, #20713 ) ;
#12533=DIRECTION ( 'NONE',  ( 0.000000000000000000, 0.000000000000000000, 1.000000000000000000 ) ) ;
#12576=CARTESIAN_POINT ( 'NONE',  ( 0.000000000000000000, -1.178949249685214307, 2.042000000000001592 ) ) ;
#12579=VECTOR ( 'NONE', #5257, 1000.000000000000000 ) ;
#12581=CARTESIAN_POINT ( 'NONE',  ( 5.000000000000000888, 4.250000000000000000, 0.000000000000000000 ) ) ;
#12605=DIRECTION ( 'NONE',  ( -0.000000000000000000, 1.000000000000000000, 1.224646799147353207E-16 ) ) ;
#12657=CARTESIAN_POINT ( 'NONE',  ( 2.500000000000000000, 0.000000000000000000, 0.000000000000000000 ) ) ;
#12804=ORIENTED_EDGE ( 'NONE', *, *, #4255, .T. ) ;
#12815=DIRECTION ( 'NONE',  ( -1.000000000000000000, -0.000000000000000000, -0.000000000000000000 ) ) ;
#12819=VERTEX_POINT ( 'NONE', #7188 ) ;
#12829=DIRECTION ( 'NONE',  ( -0.000000000000000000, 0.000000000000000000, 1.000000000000000000 ) ) ;
#12887=EDGE_CURVE ( 'NONE', #711, #3985, #12928, .T. ) ;
#12928=CIRCLE ( 'NONE', #2059, 2.500000000000000888 ) ;
#12937=CARTESIAN_POINT ( 'NONE',  ( 0.000000000000000000, 0.000000000000000000, 0.000000000000000000 ) ) ;
#13009=FILL_AREA_STYLE ('',( #16830 ) ) ;
#13014=EDGE_CURVE ( 'NONE', #5669, #7880, #14823, .T. ) ;
#13019=LINE ( 'NONE', #13259, #1325 ) ;
#13020=CARTESIAN_POINT ( 'NONE',  ( 2.500000000000000000, -1.178949249685214307, 2.042000000000001592 ) ) ;
#13031=CARTESIAN_POINT ( 'NONE',  ( 2.500000000000000000, 2.357898499370431722, -2.818925648462311528E-15 ) ) ;
#13049=DIRECTION ( 'NONE',  ( -1.000000000000000000, -0.000000000000000000, -0.000000000000000000 ) ) ;
#13061=VECTOR ( 'NONE', #9163, 999.9999999999997726 ) ;
#13079=VECTOR ( 'NONE', #3162, 1000.000000000000000 ) ;
#13089=EDGE_CURVE ( 'NONE', #6451, #18839, #22871, .T. ) ;
#13154=VECTOR ( 'NONE', #16161, 1000.000000000000114 ) ;
#13160=ORIENTED_EDGE ( 'NONE', *, *, #13496, .F. ) ;
#13169=CARTESIAN_POINT ( 'NONE',  ( 2.500000000000000000, -2.629050547790028551E-15, -2.041999999999999815 ) ) ;
#13243=ORIENTED_EDGE ( 'NONE', *, *, #13089, .F. ) ;
#13259=CARTESIAN_POINT ( 'NONE',  ( 2.500000000000000000, 2.357898499370431722, -2.818925648462311528E-15 ) ) ;
#13277=ORIENTED_EDGE ( 'NONE', *, *, #4460, .T. ) ;
#13317=CARTESIAN_POINT ( 'NONE',  ( 2.500000000000000000, 0.000000000000000000, 0.000000000000000000 ) ) ;
#13358=DIRECTION ( 'NONE',  ( 0.000000000000000000, 0.000000000000000000, -1.000000000000000000 ) ) ;
#13372=FACE_OUTER_BOUND ( 'NONE', #7809, .T. ) ;
#13446=VECTOR ( 'NONE', #10118, 1000.000000000000114 ) ;
#13496=EDGE_CURVE ( 'NONE', #19782, #16311, #978, .T. ) ;
#13518=VECTOR ( 'NONE', #2357, 1000.000000000000114 ) ;
#13523=CONICAL_SURFACE ( 'NONE', #21575, 2.041999999999999815, 1.047197551196591858 ) ;
#13588=ORIENTED_EDGE ( 'NONE', *, *, #23484, .T. ) ;
#13660=ORIENTED_EDGE ( 'NONE', *, *, #2170, .F. ) ;
#13671=ORIENTED_EDGE ( 'NONE', *, *, #18205, .F. ) ;
#13738=CARTESIAN_POINT ( 'NONE',  ( 21.00000000000000355, 0.000000000000000000, 0.000000000000000000 ) ) ;
#13752=DIRECTION ( 'NONE',  ( -1.000000000000000000, -0.000000000000000000, -0.000000000000000000 ) ) ;
#13796=CARTESIAN_POINT ( 'NONE',  ( 2.500000000000000000, 2.357898499370431722, -2.818925648462311528E-15 ) ) ;
#13815=ORIENTED_EDGE ( 'NONE', *, *, #14759, .F. ) ;
#13816=DIRECTION ( 'NONE',  ( 0.000000000000000000, -1.287488025362403787E-15, -1.000000000000000000 ) ) ;
#13817=EDGE_LOOP ( 'NONE', ( #2289, #20214, #17863, #22187 ) ) ;
#13884=TOROIDAL_SURFACE ( 'NONE', #18146, 4.000000000000000000, 0.2500000000000000000 ) ;
#13896=EDGE_CURVE ( 'NONE', #3985, #19527, #16793, .T. ) ;
#13903=CARTESIAN_POINT ( 'NONE',  ( 2.500000000000000000, 2.357898499370431722, -2.818925648462311528E-15 ) ) ;
#13954=DIRECTION ( 'NONE',  ( 0.000000000000000000, 0.000000000000000000, 1.000000000000000000 ) ) ;
#13963=ORIENTED_EDGE ( 'NONE', *, *, #2358, .F. ) ;
#14028=EDGE_LOOP ( 'NONE', ( #2799, #10598, #16939, #2527, #15853 ) ) ;
#14046=VERTEX_POINT ( 'NONE', #6172 ) ;
#14084=VERTEX_POINT ( 'NONE', #7858 ) ;
#14180=DIRECTION ( 'NONE',  ( 0.000000000000000000, 0.4999999999999990008, -0.8660254037844391517 ) ) ;
#14195=DIRECTION ( 'NONE',  ( 0.000000000000000000, 0.5000000000000009992, 0.8660254037844380415 ) ) ;
#14228=EDGE_CURVE ( 'NONE', #16080, #19722, #23006, .T. ) ;
#14259=ADVANCED_FACE ( 'NONE', ( #18919 ), #13523, .F. ) ;
#14298=VECTOR ( 'NONE', #1819, 1000.000000000000000 ) ;
#14303=CARTESIAN_POINT ( 'NONE',  ( 21.00000000000000000, 2.055000000000000160, 0.000000000000000000 ) ) ;
#14314=AXIS2_PLACEMENT_3D ( 'NONE', #13903, #8425, #21231 ) ;
#14319=CARTESIAN_POINT ( 'NONE',  ( 0.2500000000000002220, 5.204748896376250699E-16, -4.250000000000000000 ) ) ;
#14341=CARTESIAN_POINT ( 'NONE',  ( 2.500000000000000000, 0.000000000000000000, 0.000000000000000000 ) ) ;
#14388=ORIENTED_EDGE ( 'NONE', *, *, #23742, .F. ) ;
#14436=VERTEX_POINT ( 'NONE', #19504 ) ;
#14444=DIRECTION ( 'NONE',  ( 0.000000000000000000, 0.000000000000000000, 1.000000000000000000 ) ) ;
#14518=CARTESIAN_POINT ( 'NONE',  ( 0.000000000000000000, 0.000000000000000000, 4.000000000000000000 ) ) ;
#14571=CARTESIAN_POINT ( 'NONE',  ( 21.00000000000000355, 2.789133085058097101E-16, -2.055000000000000160 ) ) ;
#14587=ORIENTED_EDGE ( 'NONE', *, *, #22227, .T. ) ;
#14600=AXIS2_PLACEMENT_3D ( 'NONE', #7433, #5395, #3456 ) ;
#14615=AXIS2_PLACEMENT_3D ( 'NONE', #10978, #12815, #85 ) ;
#14657=CIRCLE ( 'NONE', #35, 2.041999999999999815 ) ;
#14687=( NAMED_UNIT ( * ) PLANE_ANGLE_UNIT ( ) SI_UNIT ( $, .RADIAN. ) );
#14698=LINE ( 'NONE', #13020, #23115 ) ;
#14725=FACE_OUTER_BOUND ( 'NONE', #7414, .T. ) ;
#14759=EDGE_CURVE ( 'NONE', #16847, #1157, #20122, .T. ) ;
#14773=ADVANCED_FACE ( 'NONE', ( #9031 ), #22357, .F. ) ;
#14797=SHAPE_REPRESENTATION_RELATIONSHIP ( 'NONE' , 'NONE' ,  #6236, #15670 ) ;
#14810=DIRECTION ( 'NONE',  ( 0.000000000000000000, 0.4999999999999992784, -0.8660254037844389297 ) ) ;
#14823=LINE ( 'NONE', #2108, #4383 ) ;
#14831=DIRECTION ( 'NONE',  ( 1.000000000000000000, 0.000000000000000000, 0.000000000000000000 ) ) ;
#14914=DIRECTION ( 'NONE',  ( 0.000000000000000000, 0.000000000000000000, 1.000000000000000000 ) ) ;
#14958=CARTESIAN_POINT ( 'NONE',  ( 0.000000000000000000, 1.178949249685212974, -2.042000000000001148 ) ) ;
#14991=DIRECTION ( 'NONE',  ( 0.000000000000000000, 0.000000000000000000, 1.000000000000000000 ) ) ;
#15002=CARTESIAN_POINT ( 'NONE',  ( -31.74999999999995737, 0.000000000000000000, 2.500000000000000444 ) ) ;
#15054=FACE_OUTER_BOUND ( 'NONE', #21850, .T. ) ;
#15072=LINE ( 'NONE', #200, #21552 ) ;
#15081=ORIENTED_EDGE ( 'NONE', *, *, #3872, .F. ) ;
#15109=UNCERTAINTY_MEASURE_WITH_UNIT (LENGTH_MEASURE( 1.000000000000000082E-05 ), #10843, 'distance_accuracy_value', 'NONE');
#15148=EDGE_LOOP ( 'NONE', ( #21348, #23689, #7401, #5333 ) ) ;
#15211=EDGE_CURVE ( 'NONE', #15625, #7880, #5412, .T. ) ;
#15216=ORIENTED_EDGE ( 'NONE', *, *, #7996, .F. ) ;
#15255=CARTESIAN_POINT ( 'NONE',  ( 0.000000000000000000, -1.178949249685214307, 2.042000000000001592 ) ) ;
#15267=CARTESIAN_POINT ( 'NONE',  ( 0.000000000000000000, -2.357898499370432166, 3.035766082959412415E-15 ) ) ;
#15268=STYLED_ITEM('',(#23927),#4664);
#15334=EDGE_LOOP ( 'NONE', ( #3566, #8205, #19355, #1682, #21803 ) ) ;
#15341=ORIENTED_EDGE ( 'NONE', *, *, #21541, .F. ) ;
#15360=ORIENTED_EDGE ( 'NONE', *, *, #7190, .F. ) ;
#15362=AXIS2_PLACEMENT_3D ( 'NONE', #17559, #8387, #12533 ) ;
#15412=CARTESIAN_POINT ( 'NONE',  ( 2.500000000000000000, -2.357898499370432166, 3.035766082959412415E-15 ) ) ;
#15417=VECTOR ( 'NONE', #21041, 1000.000000000000000 ) ;
#15471=CARTESIAN_POINT ( 'NONE',  ( 2.500000000000000000, -1.178949249685214307, 2.042000000000001592 ) ) ;
#15560=EDGE_CURVE ( 'NONE', #14084, #7880, #23577, .T. ) ;
#15565=DIRECTION ( 'NONE',  ( 0.000000000000000000, 0.000000000000000000, 1.000000000000000000 ) ) ;
#15623=CIRCLE ( 'NONE', #19443, 4.250000000000000000 ) ;
#15625=VERTEX_POINT ( 'NONE', #8613 ) ;
#15633=CYLINDRICAL_SURFACE ( 'NONE', #6160, 2.500000000000000444 ) ;
#15652=ORIENTED_EDGE ( 'NONE', *, *, #522, .F. ) ;
#15670=ADVANCED_BREP_SHAPE_REPRESENTATION ( '', ( #4664, #11210 ), #9660 ) ;
#15746=DIRECTION ( 'NONE',  ( -1.000000000000000000, -0.000000000000000000, -0.000000000000000000 ) ) ;
#15760=FACE_OUTER_BOUND ( 'NONE', #9209, .T. ) ;
#15783=ORIENTED_EDGE ( 'NONE', *, *, #32, .F. ) ;
#15793=VECTOR ( 'NONE', #18643, 1000.000000000000000 ) ;
#15817=AXIS2_PLACEMENT_3D ( 'NONE', #20446, #20308, #7641 ) ;
#15853=ORIENTED_EDGE ( 'NONE', *, *, #21712, .T. ) ;
#15884=DIRECTION ( 'NONE',  ( 0.000000000000000000, 0.8660254037844380415, -0.5000000000000009992 ) ) ;
#15909=ADVANCED_FACE ( 'NONE', ( #18092, #16293 ), #5169, .T. ) ;
#15962=CARTESIAN_POINT ( 'NONE',  ( 0.000000000000000000, -2.357898499370432166, 3.035766082959412415E-15 ) ) ;
#15988=LINE ( 'NONE', #19577, #11597 ) ;
#16016=EDGE_LOOP ( 'NONE', ( #4632, #20014, #12048, #19682, #18650 ) ) ;
#16080=VERTEX_POINT ( 'NONE', #9755 ) ;
#16082=DIRECTION ( 'NONE',  ( 0.000000000000000000, -1.000000000000000000, 1.287488025362403787E-15 ) ) ;
#16092=ORIENTED_EDGE ( 'NONE', *, *, #10682, .T. ) ;
#16093=CARTESIAN_POINT ( 'NONE',  ( 5.200000000000002842, 3.306546357697854226E-16, 2.700000000000000622 ) ) ;
#16115=ORIENTED_EDGE ( 'NONE', *, *, #4460, .F. ) ;
#16161=DIRECTION ( 'NONE',  ( 0.000000000000000000, -0.5000000000000009992, -0.8660254037844380415 ) ) ;
#16205=CIRCLE ( 'NONE', #10046, 2.500000000000000888 ) ;
#16293=FACE_OUTER_BOUND ( 'NONE', #1840, .T. ) ;
#16311=VERTEX_POINT ( 'NONE', #21789 ) ;
#16327=CIRCLE ( 'NONE', #21337, 4.000000000000000000 ) ;
#16332=DIRECTION ( 'NONE',  ( 0.000000000000000000, 1.224646799147353207E-16, 1.000000000000000000 ) ) ;
#16339=AXIS2_PLACEMENT_3D ( 'NONE', #7787, #659, #4152 ) ;
#16345=FACE_OUTER_BOUND ( 'NONE', #16016, .T. ) ;
#16401=ORIENTED_EDGE ( 'NONE', *, *, #8447, .T. ) ;
#16424=CARTESIAN_POINT ( 'NONE',  ( 0.000000000000000000, 2.357898499370431722, -2.818925648462311528E-15 ) ) ;
#16530=ADVANCED_FACE ( 'NONE', ( #13372 ), #11681, .T. ) ;
#16582=CONICAL_SURFACE ( 'NONE', #19655, 2.055000000000000160, 0.7853981633974639331 ) ;
#16607=PRESENTATION_STYLE_ASSIGNMENT (( #20201 ) ) ;
#16655=SHAPE_DEFINITION_REPRESENTATION ( #9235, #6236 ) ;
#16676=DIRECTION ( 'NONE',  ( 0.000000000000000000, 0.000000000000000000, 1.000000000000000000 ) ) ;
#16725=DIRECTION ( 'NONE',  ( 0.000000000000000000, -0.5000000000000013323, -0.8660254037844380415 ) ) ;
#16756=ORIENTED_EDGE ( 'NONE', *, *, #22785, .T. ) ;
#16776=DIRECTION ( 'NONE',  ( 0.000000000000000000, 0.000000000000000000, -1.000000000000000000 ) ) ;
#16793=LINE ( 'NONE', #15002, #1100 ) ;
#16830=FILL_AREA_STYLE_COLOUR ( '', #6934 ) ;
#16847=VERTEX_POINT ( 'NONE', #15255 ) ;
#16912=AXIS2_PLACEMENT_3D ( 'NONE', #2440, #5948, #13358 ) ;
#16939=ORIENTED_EDGE ( 'NONE', *, *, #1073, .F. ) ;
#16965=ADVANCED_FACE ( 'NONE', ( #19552 ), #17293, .F. ) ;
#17022=EDGE_CURVE ( 'NONE', #18754, #711, #8710, .T. ) ;
#17139=CARTESIAN_POINT ( 'NONE',  ( 4.999999999999997335, 5.204748896376250699E-16, -4.250000000000000000 ) ) ;
#17200=CARTESIAN_POINT ( 'NONE',  ( -31.74999999999995737, 0.000000000000000000, 0.000000000000000000 ) ) ;
#17229=EDGE_CURVE ( 'NONE', #12455, #6451, #6441, .T. ) ;
#17293=PLANE ( 'NONE',  #1413 ) ;
#17335=CARTESIAN_POINT ( 'NONE',  ( 2.500000000000000000, -2.357898499370432166, 3.035766082959412415E-15 ) ) ;
#17359=ORIENTED_EDGE ( 'NONE', *, *, #2551, .F. ) ;
#17367=CARTESIAN_POINT ( 'NONE',  ( 20.55500000000001748, 3.061616997868384127E-16, -2.500000000000000888 ) ) ;
#17370=CARTESIAN_POINT ( 'NONE',  ( 2.500000000000000000, 2.357898499370431722, -2.818925648462311528E-15 ) ) ;
#17388=DIRECTION ( 'NONE',  ( 0.000000000000000000, 0.000000000000000000, 1.000000000000000000 ) ) ;
#17488=ORIENTED_EDGE ( 'NONE', *, *, #22192, .T. ) ;
#17507=DIRECTION ( 'NONE',  ( 0.000000000000000000, -1.224646799147353454E-16, 1.000000000000000000 ) ) ;
#17529=CARTESIAN_POINT ( 'NONE',  ( 2.500000000000000000, 2.357898499370431722, -2.818925648462311528E-15 ) ) ;
#17559=CARTESIAN_POINT ( 'NONE',  ( 4.999999999999997335, 0.000000000000000000, 0.000000000000000000 ) ) ;
#17628=AXIS2_PLACEMENT_3D ( 'NONE', #16093, #20283, #16332 ) ;
#17632=DIRECTION ( 'NONE',  ( 0.000000000000000000, -1.000000000000000000, 0.000000000000000000 ) ) ;
#17662=ORIENTED_EDGE ( 'NONE', *, *, #21541, .T. ) ;
#17707=AXIS2_PLACEMENT_3D ( 'NONE', #1483, #11051, #20183 ) ;
#17737=ADVANCED_FACE ( 'NONE', ( #12161 ), #21407, .T. ) ;
#17749=AXIS2_PLACEMENT_3D ( 'NONE', #7184, #80, #23619 ) ;
#17760=AXIS2_PLACEMENT_3D ( 'NONE', #14303, #4974, #10671 ) ;
#17789=CARTESIAN_POINT ( 'NONE',  ( -31.74999999999995737, 5.204748896376250699E-16, -4.250000000000000000 ) ) ;
#17863=ORIENTED_EDGE ( 'NONE', *, *, #19170, .F. ) ;
#17938=AXIS2_PLACEMENT_3D ( 'NONE', #13796, #21120, #4577 ) ;
#18004=DIRECTION ( 'NONE',  ( 1.000000000000000000, 0.000000000000000000, 0.000000000000000000 ) ) ;
#18008=ORIENTED_EDGE ( 'NONE', *, *, #19298, .T. ) ;
#18044=EDGE_CURVE ( 'NONE', #20235, #19527, #9181, .T. ) ;
#18092=FACE_BOUND ( 'NONE', #10523, .T. ) ;
#18112=DIRECTION ( 'NONE',  ( 0.000000000000000000, 0.8660254037844380415, -0.5000000000000012212 ) ) ;
#18146=AXIS2_PLACEMENT_3D ( 'NONE', #1191, #19075, #9932 ) ;
#18201=ORIENTED_EDGE ( 'NONE', *, *, #13089, .T. ) ;
#18204=ADVANCED_FACE ( 'NONE', ( #6543 ), #19460, .T. ) ;
#18205=EDGE_CURVE ( 'NONE', #10923, #20782, #968, .T. ) ;
#18233=LINE ( 'NONE', #124, #9067 ) ;
#18246=VERTEX_POINT ( 'NONE', #15471 ) ;
#18258=CARTESIAN_POINT ( 'NONE',  ( 2.500000000000000000, 1.768423874527823791, 1.020999999999998353 ) ) ;
#18310=ORIENTED_EDGE ( 'NONE', *, *, #15211, .F. ) ;
#18329=FACE_OUTER_BOUND ( 'NONE', #11912, .T. ) ;
#18349=DIRECTION ( 'NONE',  ( -1.000000000000000000, -0.000000000000000000, -0.000000000000000000 ) ) ;
#18387=PLANE ( 'NONE',  #8019 ) ;
#18411=AXIS2_PLACEMENT_3D ( 'NONE', #3887, #11296, #18603 ) ;
#18456=PRODUCT_DEFINITION_CONTEXT ( 'detailed design', #7365, 'design' ) ;
#18473=AXIS2_PLACEMENT_3D ( 'NONE', #6435, #19457, #8113 ) ;
#18518=( LENGTH_UNIT ( ) NAMED_UNIT ( * ) SI_UNIT ( .MILLI., .METRE. ) );
#18533=( LENGTH_UNIT ( ) NAMED_UNIT ( * ) SI_UNIT ( .MILLI., .METRE. ) );
#18534=CARTESIAN_POINT ( 'NONE',  ( 2.500000000000000000, 2.629050547790028946E-15, 2.042000000000000259 ) ) ;
#18562=EDGE_LOOP ( 'NONE', ( #18008, #9191, #18310 ) ) ;
#18603=DIRECTION ( 'NONE',  ( 0.000000000000000000, 0.000000000000000000, -1.000000000000000000 ) ) ;
#18628=DIRECTION ( 'NONE',  ( 0.000000000000000000, -0.8660254037844390407, -0.4999999999999993339 ) ) ;
#18643=DIRECTION ( 'NONE',  ( 0.000000000000000000, -0.4999999999999993339, 0.8660254037844390407 ) ) ;
#18650=ORIENTED_EDGE ( 'NONE', *, *, #15211, .T. ) ;
#18690=CLOSED_SHELL ( 'NONE', ( #14259, #10820, #14773, #18204, #8052, #16530, #1618, #4931, #15909, #10778, #3701, #5362, #10361, #10019, #3628, #19804, #17737, #19060, #16965, #5921, #9328, #1557, #174, #7012, #11103, #6204, #3884 ) ) ;
#18754=VERTEX_POINT ( 'NONE', #14571 ) ;
#18782=DIRECTION ( 'NONE',  ( 0.000000000000000000, 0.000000000000000000, -1.000000000000000000 ) ) ;
#18791=ORIENTED_EDGE ( 'NONE', *, *, #8004, .F. ) ;
#18816=LINE ( 'NONE', #494, #12384 ) ;
#18839=VERTEX_POINT ( 'NONE', #15412 ) ;
#18854=EDGE_LOOP ( 'NONE', ( #15783, #13160, #8248, #22774, #9028 ) ) ;
#18861=( GEOMETRIC_REPRESENTATION_CONTEXT ( 3 ) GLOBAL_UNCERTAINTY_ASSIGNED_CONTEXT ( ( #7364 ) ) GLOBAL_UNIT_ASSIGNED_CONTEXT ( ( #18518, #14687, #2086 ) ) REPRESENTATION_CONTEXT ( 'NONE', 'WORKASPACE' ) );
#18895=EDGE_CURVE ( 'NONE', #10923, #286, #1742, .T. ) ;
#18919=FACE_OUTER_BOUND ( 'NONE', #15334, .T. ) ;
#18971=ORIENTED_EDGE ( 'NONE', *, *, #21673, .T. ) ;
#19060=ADVANCED_FACE ( 'NONE', ( #15760 ), #23105, .T. ) ;
#19068=CARTESIAN_POINT ( 'NONE',  ( 0.2500000000000002220, 0.000000000000000000, 4.250000000000000000 ) ) ;
#19074=EDGE_LOOP ( 'NONE', ( #15360, #16115 ) ) ;
#19075=DIRECTION ( 'NONE',  ( -1.000000000000000000, -0.000000000000000000, -0.000000000000000000 ) ) ;
#19134=CARTESIAN_POINT ( 'NONE',  ( 2.500000000000000000, 0.000000000000000000, 0.000000000000000000 ) ) ;
#19170=EDGE_CURVE ( 'NONE', #3985, #711, #16205, .T. ) ;
#19200=DIRECTION ( 'NONE',  ( 0.000000000000000000, 1.000000000000000000, -1.287488025362403787E-15 ) ) ;
#19219=ORIENTED_EDGE ( 'NONE', *, *, #20881, .F. ) ;
#19298=EDGE_CURVE ( 'NONE', #15625, #14084, #18816, .T. ) ;
#19355=ORIENTED_EDGE ( 'NONE', *, *, #23742, .T. ) ;
#19356=AXIS2_PLACEMENT_3D ( 'NONE', #17370, #2495, #18782 ) ;
#19434=CARTESIAN_POINT ( 'NONE',  ( -31.74999999999995737, 0.000000000000000000, 4.250000000000000000 ) ) ;
#19443=AXIS2_PLACEMENT_3D ( 'NONE', #20327, #5854, #5613 ) ;
#19457=DIRECTION ( 'NONE',  ( -1.000000000000000000, -0.000000000000000000, -0.000000000000000000 ) ) ;
#19460=CONICAL_SURFACE ( 'NONE', #3283, 2.055000000000000160, 0.7853981633974639331 ) ;
#19484=CARTESIAN_POINT ( 'NONE',  ( -31.74999999999995737, 0.000000000000000000, 0.000000000000000000 ) ) ;
#19504=CARTESIAN_POINT ( 'NONE',  ( 5.000000000000002665, 3.306546357697854226E-16, 2.700000000000000622 ) ) ;
#19527=VERTEX_POINT ( 'NONE', #344 ) ;
#19533=ORIENTED_EDGE ( 'NONE', *, *, #18895, .T. ) ;
#19552=FACE_OUTER_BOUND ( 'NONE', #14028, .T. ) ;
#19577=CARTESIAN_POINT ( 'NONE',  ( 2.500000000000000000, -1.178949249685218748, -2.041999999999998039 ) ) ;
#19608=VECTOR ( 'NONE', #12143, 1000.000000000000000 ) ;
#19655=AXIS2_PLACEMENT_3D ( 'NONE', #13738, #11802, #2711 ) ;
#19682=ORIENTED_EDGE ( 'NONE', *, *, #20881, .T. ) ;
#19722=VERTEX_POINT ( 'NONE', #12456 ) ;
#19724=CYLINDRICAL_SURFACE ( 'NONE', #2540, 4.250000000000000000 ) ;
#19725=EDGE_LOOP ( 'NONE', ( #5321, #17359, #6242 ) ) ;
#19735=( NAMED_UNIT ( * ) PLANE_ANGLE_UNIT ( ) SI_UNIT ( $, .RADIAN. ) );
#19782=VERTEX_POINT ( 'NONE', #13031 ) ;
#19792=CARTESIAN_POINT ( 'NONE',  ( 21.00000000000000355, 0.000000000000000000, 0.000000000000000000 ) ) ;
#19804=ADVANCED_FACE ( 'NONE', ( #10866 ), #7077, .F. ) ;
#19821=CARTESIAN_POINT ( 'NONE',  ( 2.500000000000000000, 1.178949249685212974, -2.042000000000001148 ) ) ;
#19850=AXIS2_PLACEMENT_3D ( 'NONE', #13317, #489, #14991 ) ;
#19972=DIRECTION ( 'NONE',  ( 0.000000000000000000, 0.000000000000000000, 1.000000000000000000 ) ) ;
#20014=ORIENTED_EDGE ( 'NONE', *, *, #20563, .T. ) ;
#20084=ORIENTED_EDGE ( 'NONE', *, *, #1145, .T. ) ;
#20122=LINE ( 'NONE', #12576, #13154 ) ;
#20183=DIRECTION ( 'NONE',  ( 0.000000000000000000, 0.000000000000000000, 1.000000000000000000 ) ) ;
#20194=PRODUCT ( 'socket head cap screw_iso_ISO 4762 M5 x 16 - 16N', 'socket head cap screw_iso_ISO 4762 M5 x 16 - 16N', '', ( #7357 ) ) ;
#20200=EDGE_CURVE ( 'NONE', #1157, #12819, #11535, .T. ) ;
#20201=SURFACE_STYLE_USAGE ( .BOTH. , #7776 ) ;
#20214=ORIENTED_EDGE ( 'NONE', *, *, #17022, .T. ) ;
#20235=VERTEX_POINT ( 'NONE', #22240 ) ;
#20272=DIRECTION ( 'NONE',  ( 0.000000000000000000, 1.000000000000000000, -1.287488025362403787E-15 ) ) ;
#20283=DIRECTION ( 'NONE',  ( 0.000000000000000000, 1.000000000000000000, -1.224646799147353207E-16 ) ) ;
#20286=ORIENTED_EDGE ( 'NONE', *, *, #21494, .F. ) ;
#20308=DIRECTION ( 'NONE',  ( 1.000000000000000000, 0.000000000000000000, 0.000000000000000000 ) ) ;
#20327=CARTESIAN_POINT ( 'NONE',  ( 0.2500000000000002220, 0.000000000000000000, 0.000000000000000000 ) ) ;
#20329=CARTESIAN_POINT ( 'NONE',  ( 4.999999999999997335, 0.000000000000000000, 0.000000000000000000 ) ) ;
#20446=CARTESIAN_POINT ( 'NONE',  ( 5.200000000000002842, 0.000000000000000000, 0.000000000000000000 ) ) ;
#20468=DIRECTION ( 'NONE',  ( 0.000000000000000000, 0.000000000000000000, 1.000000000000000000 ) ) ;
#20563=EDGE_CURVE ( 'NONE', #5669, #12251, #11386, .T. ) ;
#20576=ORIENTED_EDGE ( 'NONE', *, *, #8678, .F. ) ;
#20691=FACE_OUTER_BOUND ( 'NONE', #1428, .T. ) ;
#20713=VECTOR ( 'NONE', #21993, 1000.000000000000000 ) ;
#20777=ORIENTED_EDGE ( 'NONE', *, *, #13496, .T. ) ;
#20782=VERTEX_POINT ( 'NONE', #19068 ) ;
#20881=EDGE_CURVE ( 'NONE', #3909, #15625, #10388, .T. ) ;
#20884=FACE_OUTER_BOUND ( 'NONE', #4505, .T. ) ;
#20933=AXIS2_PLACEMENT_3D ( 'NONE', #19792, #21368, #4952 ) ;
#20964=ORIENTED_EDGE ( 'NONE', *, *, #22470, .F. ) ;
#21041=DIRECTION ( 'NONE',  ( -1.000000000000000000, -0.000000000000000000, -0.000000000000000000 ) ) ;
#21050=CARTESIAN_POINT ( 'NONE',  ( -31.74999999999995737, 0.000000000000000000, 0.000000000000000000 ) ) ;
#21120=DIRECTION ( 'NONE',  ( 1.000000000000000000, 0.000000000000000000, 0.000000000000000000 ) ) ;
#21231=DIRECTION ( 'NONE',  ( 0.000000000000000000, 0.000000000000000000, -1.000000000000000000 ) ) ;
#21316=FACE_OUTER_BOUND ( 'NONE', #6991, .T. ) ;
#21337=AXIS2_PLACEMENT_3D ( 'NONE', #4412, #10222, #22875 ) ;
#21348=ORIENTED_EDGE ( 'NONE', *, *, #7617, .F. ) ;
#21362=ORIENTED_EDGE ( 'NONE', *, *, #1145, .F. ) ;
#21368=DIRECTION ( 'NONE',  ( -1.000000000000000000, -0.000000000000000000, -0.000000000000000000 ) ) ;
#21379=VECTOR ( 'NONE', #8174, 1000.000000000000114 ) ;
#21407=PLANE ( 'NONE',  #8793 ) ;
#21427=DIRECTION ( 'NONE',  ( -1.000000000000000000, -0.000000000000000000, -0.000000000000000000 ) ) ;
#21494=EDGE_CURVE ( 'NONE', #18839, #12455, #6309, .T. ) ;
#21541=EDGE_CURVE ( 'NONE', #286, #9681, #1349, .T. ) ;
#21552=VECTOR ( 'NONE', #7554, 1000.000000000000114 ) ;
#21567=LINE ( 'NONE', #5035, #12579 ) ;
#21575=AXIS2_PLACEMENT_3D ( 'NONE', #11841, #6608, #15565 ) ;
#21587=DIRECTION ( 'NONE',  ( -1.000000000000000000, -0.000000000000000000, -0.000000000000000000 ) ) ;
#21673=EDGE_CURVE ( 'NONE', #19527, #14436, #3743, .T. ) ;
#21697=DIRECTION ( 'NONE',  ( 0.000000000000000000, 0.000000000000000000, 1.000000000000000000 ) ) ;
#21705=CARTESIAN_POINT ( 'NONE',  ( 5.200000000000002842, 0.000000000000000000, 0.000000000000000000 ) ) ;
#21712=EDGE_CURVE ( 'NONE', #14084, #1754, #12511, .T. ) ;
#21769=CARTESIAN_POINT ( 'NONE',  ( 20.55500000000001748, 0.000000000000000000, 2.500000000000000888 ) ) ;
#21789=CARTESIAN_POINT ( 'NONE',  ( 0.000000000000000000, 2.357898499370431722, -2.818925648462311528E-15 ) ) ;
#21803=ORIENTED_EDGE ( 'NONE', *, *, #8004, .T. ) ;
#21820=AXIS2_PLACEMENT_3D ( 'NONE', #20329, #3788, #11692 ) ;
#21824=VERTEX_POINT ( 'NONE', #253 ) ;
#21842=EDGE_CURVE ( 'NONE', #16311, #1754, #10890, .T. ) ;
#21848=VECTOR ( 'NONE', #8829, 1000.000000000000114 ) ;
#21850=EDGE_LOOP ( 'NONE', ( #9169, #13277, #2237, #6695 ) ) ;
#21862=AXIS2_PLACEMENT_3D ( 'NONE', #5547, #3720, #1920 ) ;
#21964=EDGE_LOOP ( 'NONE', ( #21996, #8286, #2176, #765, #7791, #7268 ) ) ;
#21993=DIRECTION ( 'NONE',  ( -1.000000000000000000, -0.000000000000000000, -0.000000000000000000 ) ) ;
#21996=ORIENTED_EDGE ( 'NONE', *, *, #32, .T. ) ;
#22033=EDGE_LOOP ( 'NONE', ( #3583, #4942, #17488, #49 ) ) ;
#22046=CARTESIAN_POINT ( 'NONE',  ( 2.500000000000000000, 2.357898499370431722, -2.818925648462311528E-15 ) ) ;
#22163=CIRCLE ( 'NONE', #11037, 2.055000000000000160 ) ;
#22164=VECTOR ( 'NONE', #23775, 1000.000000000000000 ) ;
#22187=ORIENTED_EDGE ( 'NONE', *, *, #9220, .F. ) ;
#22191=AXIS2_PLACEMENT_3D ( 'NONE', #6888, #17632, #5089 ) ;
#22192=EDGE_CURVE ( 'NONE', #20235, #3630, #8420, .T. ) ;
#22227=EDGE_CURVE ( 'NONE', #8057, #4317, #8024, .T. ) ;
#22240=CARTESIAN_POINT ( 'NONE',  ( 5.200000000000002842, 3.061616997868383634E-16, -2.500000000000000444 ) ) ;
#22334=ORIENTED_EDGE ( 'NONE', *, *, #22192, .F. ) ;
#22357=TOROIDAL_SURFACE ( 'NONE', #7696, 2.700000000000000622, 0.2000000000000000111 ) ;
#22417=CARTESIAN_POINT ( 'NONE',  ( 2.500000000000000000, -2.357898499370432166, 3.035766082959412415E-15 ) ) ;
#22470=EDGE_CURVE ( 'NONE', #286, #10923, #1829, .T. ) ;
#22571=CARTESIAN_POINT ( 'NONE',  ( 2.500000000000000000, 0.000000000000000000, 2.041999999999999815 ) ) ;
#22600=DIRECTION ( 'NONE',  ( 0.000000000000000000, 0.4999999999999990008, -0.8660254037844391517 ) ) ;
#22617=AXIS2_PLACEMENT_3D ( 'NONE', #7010, #12605, #17507 ) ;
#22633=LINE ( 'NONE', #311, #13518 ) ;
#22774=ORIENTED_EDGE ( 'NONE', *, *, #2551, .T. ) ;
#22785=EDGE_CURVE ( 'NONE', #3630, #14436, #10368, .T. ) ;
#22789=CARTESIAN_POINT ( 'NONE',  ( 2.500000000000000000, 1.178949249685217415, 2.041999999999998483 ) ) ;
#22805=EDGE_LOOP ( 'NONE', ( #4914, #16401, #15216, #21362 ) ) ;
#22840=VECTOR ( 'NONE', #8668, 1000.000000000000000 ) ;
#22871=LINE ( 'NONE', #9984, #21379 ) ;
#22875=DIRECTION ( 'NONE',  ( 0.000000000000000000, 0.000000000000000000, 1.000000000000000000 ) ) ;
#22917=FACE_OUTER_BOUND ( 'NONE', #5208, .T. ) ;
#22927=CARTESIAN_POINT ( 'NONE',  ( 4.999999999999997335, 0.000000000000000000, 4.250000000000000000 ) ) ;
#23006=LINE ( 'NONE', #22789, #11967 ) ;
#23027=AXIS2_PLACEMENT_3D ( 'NONE', #10028, #9904, #17388 ) ;
#23105=PLANE ( 'NONE',  #6935 ) ;
#23115=VECTOR ( 'NONE', #5494, 1000.000000000000000 ) ;
#23126=EDGE_LOOP ( 'NONE', ( #23707, #20576, #20084, #7704 ) ) ;
#23135=AXIS2_PLACEMENT_3D ( 'NONE', #12657, #3431, #19972 ) ;
#23156=LINE ( 'NONE', #11980, #22840 ) ;
#23199=PLANE ( 'NONE',  #17760 ) ;
#23285=ORIENTED_EDGE ( 'NONE', *, *, #18895, .F. ) ;
#23326=ORIENTED_EDGE ( 'NONE', *, *, #13896, .F. ) ;
#23345=AXIS2_PLACEMENT_3D ( 'NONE', #7959, #4209, #16776 ) ;
#23370=EDGE_CURVE ( 'NONE', #19782, #3909, #9142, .T. ) ;
#23484=EDGE_CURVE ( 'NONE', #12455, #21824, #15072, .T. ) ;
#23490=FACE_OUTER_BOUND ( 'NONE', #22033, .T. ) ;
#23503=EDGE_LOOP ( 'NONE', ( #15341, #4304, #873, #23569 ) ) ;
#23537=PLANE ( 'NONE',  #9847 ) ;
#23569=ORIENTED_EDGE ( 'NONE', *, *, #8678, .T. ) ;
#23577=LINE ( 'NONE', #6796, #13079 ) ;
#23619=DIRECTION ( 'NONE',  ( 0.000000000000000000, -1.000000000000000000, 1.287488025362403787E-15 ) ) ;
#23626=DIRECTION ( 'NONE',  ( -1.000000000000000000, -0.000000000000000000, -0.000000000000000000 ) ) ;
#23628=ORIENTED_EDGE ( 'NONE', *, *, #10968, .T. ) ;
#23689=ORIENTED_EDGE ( 'NONE', *, *, #12887, .T. ) ;
#23694=ORIENTED_EDGE ( 'NONE', *, *, #20200, .F. ) ;
#23707=ORIENTED_EDGE ( 'NONE', *, *, #8447, .F. ) ;
#23742=EDGE_CURVE ( 'NONE', #7880, #12455, #14657, .T. ) ;
#23748=ORIENTED_EDGE ( 'NONE', *, *, #17229, .F. ) ;
#23775=DIRECTION ( 'NONE',  ( 0.000000000000000000, -0.4999999999999993339, 0.8660254037844390407 ) ) ;
#23921=COLOUR_RGB('Black',0.12,0.14,0.17);
#23922=FILL_AREA_STYLE_COLOUR('',#23921);
#23923=FILL_AREA_STYLE('',(#23922));
#23924=SURFACE_STYLE_FILL_AREA(#23923);
#23925=SURFACE_SIDE_STYLE('',(#23924));
#23926=SURFACE_STYLE_USAGE(.BOTH.,#23925);
#23927=PRESENTATION_STYLE_ASSIGNMENT((#23926));
ENDSEC;
END-ISO-10303-21;
